ISO-10303-21;
HEADER;
/* Generated by software containing ST-Developer
 * from STEP Tools, Inc. (www.steptools.com) 
 */

FILE_DESCRIPTION(
/* description */ ('Belt-driven linear axis on 2020 extrusion'),
/* implementation_level */ '2;1');

FILE_NAME(
/* name */ 'M5x17.5 extrusion screw.step',
/* time_stamp */ '2026-10-28T03:26:09-07:00',
/* author */ (''),
/* organization */ (''),
/* preprocessor_version */ 'ST-DEVELOPER v20.2',
/* originating_system */ 'Autodesk Translation Framework v15.17.0.0',
/* authorisation */ '');

FILE_SCHEMA (('AUTOMOTIVE_DESIGN { 1 0 10303 214 3 1 1 }'));
ENDSEC;

DATA;
#10=MECHANICAL_DESIGN_GEOMETRIC_PRESENTATION_REPRESENTATION('',(#641),#20096);
#11=ORIENTED_CLOSED_SHELL('',*,#10954,.F.);
#15=BREP_WITH_VOIDS('Body1',#10955,(#11));
#501=CONICAL_SURFACE('',#12134,0.4,0.785398163397448);
#502=CONICAL_SURFACE('',#12138,0.41,0.785398163397448);
#503=CONICAL_SURFACE('',#12142,0.26,0.463647609000806);
#539=SHAPE_REPRESENTATION_RELATIONSHIP('SRR','None',#20336,#585);
#585=ADVANCED_BREP_SHAPE_REPRESENTATION('',(#15),#20067);
#641=STYLED_ITEM('',(#20657),#15);
#816=FACE_BOUND('',#2310,.T.);
#1081=PLANE('',#12122);
#1082=PLANE('',#12123);
#1083=PLANE('',#12124);
#1084=PLANE('',#12125);
#1085=PLANE('',#12126);
#1086=PLANE('',#12127);
#1087=PLANE('',#12128);
#1088=PLANE('',#12129);
#1089=PLANE('',#12130);
#1090=PLANE('',#12132);
#1091=PLANE('',#12140);
#1576=FACE_OUTER_BOUND('',#2296,.T.);
#1577=FACE_OUTER_BOUND('',#2297,.T.);
#1578=FACE_OUTER_BOUND('',#2298,.T.);
#1579=FACE_OUTER_BOUND('',#2299,.T.);
#1580=FACE_OUTER_BOUND('',#2300,.T.);
#1581=FACE_OUTER_BOUND('',#2301,.T.);
#1582=FACE_OUTER_BOUND('',#2302,.T.);
#1583=FACE_OUTER_BOUND('',#2303,.T.);
#1584=FACE_OUTER_BOUND('',#2304,.T.);
#1585=FACE_OUTER_BOUND('',#2305,.T.);
#1586=FACE_OUTER_BOUND('',#2306,.T.);
#1587=FACE_OUTER_BOUND('',#2307,.T.);
#1588=FACE_OUTER_BOUND('',#2308,.T.);
#1589=FACE_OUTER_BOUND('',#2309,.T.);
#1590=FACE_OUTER_BOUND('',#2311,.T.);
#1591=FACE_OUTER_BOUND('',#2312,.T.);
#2296=EDGE_LOOP('',(#8785,#8786,#8787,#8788));
#2297=EDGE_LOOP('',(#8789,#8790,#8791,#8792));
#2298=EDGE_LOOP('',(#8793,#8794,#8795,#8796));
#2299=EDGE_LOOP('',(#8797,#8798,#8799,#8800));
#2300=EDGE_LOOP('',(#8801,#8802,#8803,#8804));
#2301=EDGE_LOOP('',(#8805,#8806,#8807,#8808));
#2302=EDGE_LOOP('',(#8809,#8810,#8811,#8812,#8813,#8814));
#2303=EDGE_LOOP('',(#8815,#8816,#8817,#8818,#8819,#8820));
#2304=EDGE_LOOP('',(#8821));
#2305=EDGE_LOOP('',(#8822));
#2306=EDGE_LOOP('',(#8823,#8824,#8825,#8826));
#2307=EDGE_LOOP('',(#8827,#8828,#8829,#8830));
#2308=EDGE_LOOP('',(#8831,#8832,#8833,#8834));
#2309=EDGE_LOOP('',(#8835));
#2310=EDGE_LOOP('',(#8836));
#2311=EDGE_LOOP('',(#8837,#8838,#8839,#8840));
#2312=EDGE_LOOP('',(#8841,#8842,#8843,#8844));
#3137=LINE('',#18215,#3994);
#3138=LINE('',#18217,#3995);
#3139=LINE('',#18219,#3996);
#3140=LINE('',#18220,#3997);
#3141=LINE('',#18223,#3998);
#3142=LINE('',#18225,#3999);
#3143=LINE('',#18226,#4000);
#3144=LINE('',#18229,#4001);
#3145=LINE('',#18231,#4002);
#3146=LINE('',#18232,#4003);
#3147=LINE('',#18235,#4004);
#3148=LINE('',#18237,#4005);
#3149=LINE('',#18238,#4006);
#3150=LINE('',#18241,#4007);
#3151=LINE('',#18243,#4008);
#3152=LINE('',#18244,#4009);
#3153=LINE('',#18246,#4010);
#3154=LINE('',#18247,#4011);
#3155=LINE('',#18259,#4012);
#3156=LINE('',#18263,#4013);
#3157=LINE('',#18267,#4014);
#3158=LINE('',#18274,#4015);
#3159=LINE('',#18276,#4016);
#3994=VECTOR('',#14523,1.);
#3995=VECTOR('',#14524,1.);
#3996=VECTOR('',#14525,1.);
#3997=VECTOR('',#14526,1.);
#3998=VECTOR('',#14529,1.);
#3999=VECTOR('',#14530,1.);
#4000=VECTOR('',#14531,1.);
#4001=VECTOR('',#14534,1.);
#4002=VECTOR('',#14535,1.);
#4003=VECTOR('',#14536,1.);
#4004=VECTOR('',#14539,1.);
#4005=VECTOR('',#14540,1.);
#4006=VECTOR('',#14541,1.);
#4007=VECTOR('',#14544,1.);
#4008=VECTOR('',#14545,1.);
#4009=VECTOR('',#14546,1.);
#4010=VECTOR('',#14549,1.);
#4011=VECTOR('',#14550,1.);
#4012=VECTOR('',#14567,0.4);
#4013=VECTOR('',#14572,0.425);
#4014=VECTOR('',#14577,0.41);
#4015=VECTOR('',#14586,0.26);
#4016=VECTOR('',#14589,0.25);
#4653=CIRCLE('',#12131,0.24505);
#4654=CIRCLE('',#12133,0.375);
#4655=CIRCLE('',#12135,0.425);
#4656=CIRCLE('',#12137,0.425);
#4657=CIRCLE('',#12139,0.395);
#4658=CIRCLE('',#12141,0.27);
#4659=CIRCLE('',#12143,0.24505);
#5412=VERTEX_POINT('',#18213);
#5413=VERTEX_POINT('',#18214);
#5414=VERTEX_POINT('',#18216);
#5415=VERTEX_POINT('',#18218);
#5416=VERTEX_POINT('',#18222);
#5417=VERTEX_POINT('',#18224);
#5418=VERTEX_POINT('',#18228);
#5419=VERTEX_POINT('',#18230);
#5420=VERTEX_POINT('',#18234);
#5421=VERTEX_POINT('',#18236);
#5422=VERTEX_POINT('',#18240);
#5423=VERTEX_POINT('',#18242);
#5424=VERTEX_POINT('',#18251);
#5425=VERTEX_POINT('',#18254);
#5426=VERTEX_POINT('',#18257);
#5427=VERTEX_POINT('',#18261);
#5428=VERTEX_POINT('',#18265);
#5429=VERTEX_POINT('',#18269);
#5430=VERTEX_POINT('',#18272);
#6607=EDGE_CURVE('',#5412,#5413,#3137,.T.);
#6608=EDGE_CURVE('',#5413,#5414,#3138,.T.);
#6609=EDGE_CURVE('',#5414,#5415,#3139,.T.);
#6610=EDGE_CURVE('',#5412,#5415,#3140,.T.);
#6611=EDGE_CURVE('',#5413,#5416,#3141,.T.);
#6612=EDGE_CURVE('',#5416,#5417,#3142,.T.);
#6613=EDGE_CURVE('',#5417,#5414,#3143,.T.);
#6614=EDGE_CURVE('',#5416,#5418,#3144,.T.);
#6615=EDGE_CURVE('',#5418,#5419,#3145,.T.);
#6616=EDGE_CURVE('',#5419,#5417,#3146,.T.);
#6617=EDGE_CURVE('',#5418,#5420,#3147,.T.);
#6618=EDGE_CURVE('',#5420,#5421,#3148,.T.);
#6619=EDGE_CURVE('',#5421,#5419,#3149,.T.);
#6620=EDGE_CURVE('',#5420,#5422,#3150,.T.);
#6621=EDGE_CURVE('',#5422,#5423,#3151,.T.);
#6622=EDGE_CURVE('',#5423,#5421,#3152,.T.);
#6623=EDGE_CURVE('',#5422,#5412,#3153,.T.);
#6624=EDGE_CURVE('',#5415,#5423,#3154,.T.);
#6625=EDGE_CURVE('',#5424,#5424,#4653,.T.);
#6626=EDGE_CURVE('',#5425,#5425,#4654,.T.);
#6627=EDGE_CURVE('',#5426,#5426,#4655,.T.);
#6628=EDGE_CURVE('',#5426,#5425,#3155,.T.);
#6629=EDGE_CURVE('',#5427,#5427,#4656,.T.);
#6630=EDGE_CURVE('',#5427,#5426,#3156,.T.);
#6631=EDGE_CURVE('',#5428,#5428,#4657,.T.);
#6632=EDGE_CURVE('',#5428,#5427,#3157,.T.);
#6633=EDGE_CURVE('',#5429,#5429,#4658,.T.);
#6634=EDGE_CURVE('',#5430,#5430,#4659,.F.);
#6635=EDGE_CURVE('',#5430,#5429,#3158,.T.);
#6636=EDGE_CURVE('',#5424,#5430,#3159,.T.);
#8785=ORIENTED_EDGE('',*,*,#6607,.T.);
#8786=ORIENTED_EDGE('',*,*,#6608,.T.);
#8787=ORIENTED_EDGE('',*,*,#6609,.T.);
#8788=ORIENTED_EDGE('',*,*,#6610,.F.);
#8789=ORIENTED_EDGE('',*,*,#6611,.T.);
#8790=ORIENTED_EDGE('',*,*,#6612,.T.);
#8791=ORIENTED_EDGE('',*,*,#6613,.T.);
#8792=ORIENTED_EDGE('',*,*,#6608,.F.);
#8793=ORIENTED_EDGE('',*,*,#6614,.T.);
#8794=ORIENTED_EDGE('',*,*,#6615,.T.);
#8795=ORIENTED_EDGE('',*,*,#6616,.T.);
#8796=ORIENTED_EDGE('',*,*,#6612,.F.);
#8797=ORIENTED_EDGE('',*,*,#6617,.T.);
#8798=ORIENTED_EDGE('',*,*,#6618,.T.);
#8799=ORIENTED_EDGE('',*,*,#6619,.T.);
#8800=ORIENTED_EDGE('',*,*,#6615,.F.);
#8801=ORIENTED_EDGE('',*,*,#6620,.T.);
#8802=ORIENTED_EDGE('',*,*,#6621,.T.);
#8803=ORIENTED_EDGE('',*,*,#6622,.T.);
#8804=ORIENTED_EDGE('',*,*,#6618,.F.);
#8805=ORIENTED_EDGE('',*,*,#6623,.T.);
#8806=ORIENTED_EDGE('',*,*,#6610,.T.);
#8807=ORIENTED_EDGE('',*,*,#6624,.T.);
#8808=ORIENTED_EDGE('',*,*,#6621,.F.);
#8809=ORIENTED_EDGE('',*,*,#6623,.F.);
#8810=ORIENTED_EDGE('',*,*,#6620,.F.);
#8811=ORIENTED_EDGE('',*,*,#6617,.F.);
#8812=ORIENTED_EDGE('',*,*,#6614,.F.);
#8813=ORIENTED_EDGE('',*,*,#6611,.F.);
#8814=ORIENTED_EDGE('',*,*,#6607,.F.);
#8815=ORIENTED_EDGE('',*,*,#6624,.F.);
#8816=ORIENTED_EDGE('',*,*,#6609,.F.);
#8817=ORIENTED_EDGE('',*,*,#6613,.F.);
#8818=ORIENTED_EDGE('',*,*,#6616,.F.);
#8819=ORIENTED_EDGE('',*,*,#6619,.F.);
#8820=ORIENTED_EDGE('',*,*,#6622,.F.);
#8821=ORIENTED_EDGE('',*,*,#6625,.F.);
#8822=ORIENTED_EDGE('',*,*,#6626,.F.);
#8823=ORIENTED_EDGE('',*,*,#6627,.F.);
#8824=ORIENTED_EDGE('',*,*,#6628,.T.);
#8825=ORIENTED_EDGE('',*,*,#6626,.T.);
#8826=ORIENTED_EDGE('',*,*,#6628,.F.);
#8827=ORIENTED_EDGE('',*,*,#6629,.F.);
#8828=ORIENTED_EDGE('',*,*,#6630,.T.);
#8829=ORIENTED_EDGE('',*,*,#6627,.T.);
#8830=ORIENTED_EDGE('',*,*,#6630,.F.);
#8831=ORIENTED_EDGE('',*,*,#6631,.F.);
#8832=ORIENTED_EDGE('',*,*,#6632,.T.);
#8833=ORIENTED_EDGE('',*,*,#6629,.T.);
#8834=ORIENTED_EDGE('',*,*,#6632,.F.);
#8835=ORIENTED_EDGE('',*,*,#6631,.T.);
#8836=ORIENTED_EDGE('',*,*,#6633,.F.);
#8837=ORIENTED_EDGE('',*,*,#6634,.F.);
#8838=ORIENTED_EDGE('',*,*,#6635,.T.);
#8839=ORIENTED_EDGE('',*,*,#6633,.T.);
#8840=ORIENTED_EDGE('',*,*,#6635,.F.);
#8841=ORIENTED_EDGE('',*,*,#6625,.T.);
#8842=ORIENTED_EDGE('',*,*,#6636,.T.);
#8843=ORIENTED_EDGE('',*,*,#6634,.T.);
#8844=ORIENTED_EDGE('',*,*,#6636,.F.);
#10189=CYLINDRICAL_SURFACE('',#12136,0.425);
#10190=CYLINDRICAL_SURFACE('',#12144,0.24505);
#10627=ADVANCED_FACE('',(#1576),#1081,.F.);
#10628=ADVANCED_FACE('',(#1577),#1082,.F.);
#10629=ADVANCED_FACE('',(#1578),#1083,.F.);
#10630=ADVANCED_FACE('',(#1579),#1084,.F.);
#10631=ADVANCED_FACE('',(#1580),#1085,.F.);
#10632=ADVANCED_FACE('',(#1581),#1086,.F.);
#10633=ADVANCED_FACE('',(#1582),#1087,.F.);
#10634=ADVANCED_FACE('',(#1583),#1088,.F.);
#10635=ADVANCED_FACE('',(#1584),#1089,.F.);
#10636=ADVANCED_FACE('',(#1585),#1090,.T.);
#10637=ADVANCED_FACE('',(#1586),#501,.T.);
#10638=ADVANCED_FACE('',(#1587),#10189,.T.);
#10639=ADVANCED_FACE('',(#1588),#502,.T.);
#10640=ADVANCED_FACE('',(#1589,#816),#1091,.T.);
#10641=ADVANCED_FACE('',(#1590),#503,.T.);
#10642=ADVANCED_FACE('',(#1591),#10190,.T.);
#10954=CLOSED_SHELL('',(#10627,#10628,#10629,#10630,#10631,#10632,#10633,
#10634));
#10955=CLOSED_SHELL('',(#10635,#10636,#10637,#10638,#10639,#10640,#10641,
#10642));
#12121=AXIS2_PLACEMENT_3D('',#18211,#14519,#14520);
#12122=AXIS2_PLACEMENT_3D('',#18212,#14521,#14522);
#12123=AXIS2_PLACEMENT_3D('',#18221,#14527,#14528);
#12124=AXIS2_PLACEMENT_3D('',#18227,#14532,#14533);
#12125=AXIS2_PLACEMENT_3D('',#18233,#14537,#14538);
#12126=AXIS2_PLACEMENT_3D('',#18239,#14542,#14543);
#12127=AXIS2_PLACEMENT_3D('',#18245,#14547,#14548);
#12128=AXIS2_PLACEMENT_3D('',#18248,#14551,#14552);
#12129=AXIS2_PLACEMENT_3D('',#18249,#14553,#14554);
#12130=AXIS2_PLACEMENT_3D('',#18250,#14555,#14556);
#12131=AXIS2_PLACEMENT_3D('',#18252,#14557,#14558);
#12132=AXIS2_PLACEMENT_3D('',#18253,#14559,#14560);
#12133=AXIS2_PLACEMENT_3D('',#18255,#14561,#14562);
#12134=AXIS2_PLACEMENT_3D('',#18256,#14563,#14564);
#12135=AXIS2_PLACEMENT_3D('',#18258,#14565,#14566);
#12136=AXIS2_PLACEMENT_3D('',#18260,#14568,#14569);
#12137=AXIS2_PLACEMENT_3D('',#18262,#14570,#14571);
#12138=AXIS2_PLACEMENT_3D('',#18264,#14573,#14574);
#12139=AXIS2_PLACEMENT_3D('',#18266,#14575,#14576);
#12140=AXIS2_PLACEMENT_3D('',#18268,#14578,#14579);
#12141=AXIS2_PLACEMENT_3D('',#18270,#14580,#14581);
#12142=AXIS2_PLACEMENT_3D('',#18271,#14582,#14583);
#12143=AXIS2_PLACEMENT_3D('',#18273,#14584,#14585);
#12144=AXIS2_PLACEMENT_3D('',#18275,#14587,#14588);
#14519=DIRECTION('axis',(0.,0.,1.));
#14520=DIRECTION('refdir',(1.,0.,0.));
#14521=DIRECTION('center_axis',(0.866025403784439,0.,-0.5));
#14522=DIRECTION('ref_axis',(0.5,0.,0.866025403784439));
#14523=DIRECTION('',(-0.5,0.,-0.866025403784439));
#14524=DIRECTION('',(0.,-1.,0.));
#14525=DIRECTION('',(0.5,0.,0.866025403784439));
#14526=DIRECTION('',(0.,-1.,0.));
#14527=DIRECTION('center_axis',(1.20185167898973E-16,0.,-1.));
#14528=DIRECTION('ref_axis',(1.,0.,1.20185167898973E-16));
#14529=DIRECTION('',(-1.,0.,-1.20185167898973E-16));
#14530=DIRECTION('',(0.,-1.,0.));
#14531=DIRECTION('',(1.,0.,1.20185167898973E-16));
#14532=DIRECTION('center_axis',(-0.866025403784439,0.,-0.5));
#14533=DIRECTION('ref_axis',(0.5,0.,-0.866025403784439));
#14534=DIRECTION('',(-0.5,0.,0.866025403784439));
#14535=DIRECTION('',(0.,-1.,0.));
#14536=DIRECTION('',(0.5,0.,-0.866025403784439));
#14537=DIRECTION('center_axis',(-0.866025403784439,0.,0.5));
#14538=DIRECTION('ref_axis',(-0.5,0.,-0.866025403784439));
#14539=DIRECTION('',(0.5,0.,0.866025403784439));
#14540=DIRECTION('',(0.,-1.,0.));
#14541=DIRECTION('',(-0.5,0.,-0.866025403784439));
#14542=DIRECTION('center_axis',(-2.40370335797945E-16,0.,1.));
#14543=DIRECTION('ref_axis',(-1.,0.,-2.40370335797945E-16));
#14544=DIRECTION('',(1.,0.,2.40370335797945E-16));
#14545=DIRECTION('',(0.,-1.,0.));
#14546=DIRECTION('',(-1.,0.,-2.40370335797945E-16));
#14547=DIRECTION('center_axis',(0.866025403784439,0.,0.5));
#14548=DIRECTION('ref_axis',(-0.5,0.,0.866025403784439));
#14549=DIRECTION('',(0.5,0.,-0.866025403784439));
#14550=DIRECTION('',(-0.5,0.,0.866025403784439));
#14551=DIRECTION('center_axis',(0.,1.,0.));
#14552=DIRECTION('ref_axis',(1.,0.,0.));
#14553=DIRECTION('center_axis',(0.,-1.,0.));
#14554=DIRECTION('ref_axis',(0.,0.,-1.));
#14555=DIRECTION('center_axis',(0.,1.,0.));
#14556=DIRECTION('ref_axis',(1.,0.,0.));
#14557=DIRECTION('center_axis',(0.,1.,0.));
#14558=DIRECTION('ref_axis',(1.,0.,0.));
#14559=DIRECTION('center_axis',(0.,1.,0.));
#14560=DIRECTION('ref_axis',(0.,0.,1.));
#14561=DIRECTION('center_axis',(0.,-1.,0.));
#14562=DIRECTION('ref_axis',(1.,0.,0.));
#14563=DIRECTION('center_axis',(0.,-1.,0.));
#14564=DIRECTION('ref_axis',(1.,0.,0.));
#14565=DIRECTION('center_axis',(0.,-1.,0.));
#14566=DIRECTION('ref_axis',(1.,0.,0.));
#14567=DIRECTION('',(0.707106781186548,0.707106781186547,8.65956056235493E-17));
#14568=DIRECTION('center_axis',(0.,-1.,0.));
#14569=DIRECTION('ref_axis',(1.,0.,0.));
#14570=DIRECTION('center_axis',(0.,-1.,0.));
#14571=DIRECTION('ref_axis',(1.,0.,0.));
#14572=DIRECTION('',(0.,1.,0.));
#14573=DIRECTION('center_axis',(0.,1.,0.));
#14574=DIRECTION('ref_axis',(1.,0.,0.));
#14575=DIRECTION('center_axis',(0.,-1.,0.));
#14576=DIRECTION('ref_axis',(1.,0.,0.));
#14577=DIRECTION('',(-0.707106781186547,0.707106781186548,-8.65956056235493E-17));
#14578=DIRECTION('center_axis',(0.,-1.,0.));
#14579=DIRECTION('ref_axis',(0.,0.,-1.));
#14580=DIRECTION('center_axis',(0.,-1.,0.));
#14581=DIRECTION('ref_axis',(1.,0.,0.));
#14582=DIRECTION('center_axis',(0.,1.,0.));
#14583=DIRECTION('ref_axis',(1.,0.,0.));
#14584=DIRECTION('center_axis',(0.,1.,0.));
#14585=DIRECTION('ref_axis',(1.,0.,0.));
#14586=DIRECTION('',(-0.447213595499958,0.894427190999916,-5.47678698264203E-17));
#14587=DIRECTION('center_axis',(0.,-1.,0.));
#14588=DIRECTION('ref_axis',(1.,0.,0.));
#14589=DIRECTION('',(0.,1.,0.));
#18211=CARTESIAN_POINT('',(0.,0.,0.));
#18212=CARTESIAN_POINT('Origin',(0.115470053837925,-0.5,-0.2));
#18213=CARTESIAN_POINT('',(0.23094010767585,-0.5,0.));
#18214=CARTESIAN_POINT('',(0.115470053837925,-0.5,-0.2));
#18215=CARTESIAN_POINT('',(0.23094010767585,-0.5,0.));
#18216=CARTESIAN_POINT('',(0.115470053837925,-0.8,-0.2));
#18217=CARTESIAN_POINT('',(0.115470053837925,-0.5,-0.2));
#18218=CARTESIAN_POINT('',(0.23094010767585,-0.8,0.));
#18219=CARTESIAN_POINT('',(0.23094010767585,-0.8,0.));
#18220=CARTESIAN_POINT('',(0.23094010767585,-0.5,0.));
#18221=CARTESIAN_POINT('Origin',(-0.115470053837925,-0.5,-0.2));
#18222=CARTESIAN_POINT('',(-0.115470053837925,-0.5,-0.2));
#18223=CARTESIAN_POINT('',(0.115470053837925,-0.5,-0.2));
#18224=CARTESIAN_POINT('',(-0.115470053837925,-0.8,-0.2));
#18225=CARTESIAN_POINT('',(-0.115470053837925,-0.5,-0.2));
#18226=CARTESIAN_POINT('',(0.115470053837925,-0.8,-0.2));
#18227=CARTESIAN_POINT('Origin',(-0.23094010767585,-0.5,-2.77555756156289E-17));
#18228=CARTESIAN_POINT('',(-0.23094010767585,-0.5,-2.82820063659975E-17));
#18229=CARTESIAN_POINT('',(-0.115470053837925,-0.5,-0.2));
#18230=CARTESIAN_POINT('',(-0.23094010767585,-0.8,-2.77555756156289E-17));
#18231=CARTESIAN_POINT('',(-0.23094010767585,-0.5,-2.82820063659975E-17));
#18232=CARTESIAN_POINT('',(-0.115470053837925,-0.8,-0.2));
#18233=CARTESIAN_POINT('Origin',(-0.115470053837925,-0.5,0.2));
#18234=CARTESIAN_POINT('',(-0.115470053837925,-0.5,0.2));
#18235=CARTESIAN_POINT('',(-0.23094010767585,-0.5,-2.82820063659975E-17));
#18236=CARTESIAN_POINT('',(-0.115470053837925,-0.8,0.2));
#18237=CARTESIAN_POINT('',(-0.115470053837925,-0.5,0.2));
#18238=CARTESIAN_POINT('',(-0.23094010767585,-0.8,-2.82820063659975E-17));
#18239=CARTESIAN_POINT('Origin',(0.115470053837925,-0.5,0.2));
#18240=CARTESIAN_POINT('',(0.115470053837925,-0.5,0.2));
#18241=CARTESIAN_POINT('',(-0.115470053837925,-0.5,0.2));
#18242=CARTESIAN_POINT('',(0.115470053837925,-0.8,0.2));
#18243=CARTESIAN_POINT('',(0.115470053837925,-0.5,0.2));
#18244=CARTESIAN_POINT('',(-0.115470053837925,-0.8,0.2));
#18245=CARTESIAN_POINT('Origin',(0.23094010767585,-0.5,0.));
#18246=CARTESIAN_POINT('',(0.115470053837925,-0.5,0.2));
#18247=CARTESIAN_POINT('',(0.115470053837925,-0.8,0.2));
#18248=CARTESIAN_POINT('Origin',(0.,-0.5,0.));
#18249=CARTESIAN_POINT('Origin',(0.,-0.8,0.));
#18250=CARTESIAN_POINT('Origin',(0.,-1.75,0.));
#18251=CARTESIAN_POINT('',(-0.24505,-1.75,3.00099698131059E-17));
#18252=CARTESIAN_POINT('Origin',(0.,-1.75,0.));
#18253=CARTESIAN_POINT('Origin',(0.375,0.5,0.));
#18254=CARTESIAN_POINT('',(-0.375,0.5,-4.59242549680257E-17));
#18255=CARTESIAN_POINT('Origin',(0.,0.5,0.));
#18256=CARTESIAN_POINT('Origin',(0.,0.475,0.));
#18257=CARTESIAN_POINT('',(-0.425,0.45,-5.20474889637625E-17));
#18258=CARTESIAN_POINT('Origin',(0.,0.45,0.));
#18259=CARTESIAN_POINT('',(-0.4,0.475,-4.89858719658941E-17));
#18260=CARTESIAN_POINT('Origin',(0.,0.24,0.));
#18261=CARTESIAN_POINT('',(-0.425,0.0299999999999998,-5.20474889637625E-17));
#18262=CARTESIAN_POINT('Origin',(0.,0.0299999999999998,0.));
#18263=CARTESIAN_POINT('',(-0.425,0.24,-5.20474889637625E-17));
#18264=CARTESIAN_POINT('Origin',(0.,0.0150000000000001,0.));
#18265=CARTESIAN_POINT('',(-0.395,4.85722573273506E-17,-4.83735485663204E-17));
#18266=CARTESIAN_POINT('Origin',(0.,0.,0.));
#18267=CARTESIAN_POINT('',(-0.41,0.0150000000000001,-5.02105187650415E-17));
#18268=CARTESIAN_POINT('Origin',(0.27,0.,0.));
#18269=CARTESIAN_POINT('',(-0.27,0.,-3.30654635769785E-17));
#18270=CARTESIAN_POINT('Origin',(0.,0.,0.));
#18271=CARTESIAN_POINT('Origin',(0.,-0.02,0.));
#18272=CARTESIAN_POINT('',(-0.24505,-0.0498999999999999,3.00099698131059E-17));
#18273=CARTESIAN_POINT('Origin',(0.,-0.0498999999999999,0.));
#18274=CARTESIAN_POINT('',(-0.26,-0.02,-3.18408167778312E-17));
#18275=CARTESIAN_POINT('Origin',(0.,-0.995,0.));
#18276=CARTESIAN_POINT('',(-0.24505,-0.995,-3.00099698131059E-17));
#20013=UNCERTAINTY_MEASURE_WITH_UNIT(LENGTH_MEASURE(0.001),#20097,
'DISTANCE_ACCURACY_VALUE',
'Maximum model space distance between geometric entities at asserted c
onnectivities');
#20042=UNCERTAINTY_MEASURE_WITH_UNIT(LENGTH_MEASURE(0.001),#20097,
'DISTANCE_ACCURACY_VALUE',
'Maximum model space distance between geometric entities at asserted c
onnectivities');
#20067=(
GEOMETRIC_REPRESENTATION_CONTEXT(3)
GLOBAL_UNCERTAINTY_ASSIGNED_CONTEXT((#20013))
GLOBAL_UNIT_ASSIGNED_CONTEXT((#20097,#20099,#20100))
REPRESENTATION_CONTEXT('','3D')
);
#20096=(
GEOMETRIC_REPRESENTATION_CONTEXT(3)
GLOBAL_UNCERTAINTY_ASSIGNED_CONTEXT((#20042))
GLOBAL_UNIT_ASSIGNED_CONTEXT((#20097,#20099,#20100))
REPRESENTATION_CONTEXT('','3D')
);
#20097=(
LENGTH_UNIT()
NAMED_UNIT(*)
SI_UNIT(.CENTI.,.METRE.)
);
#20099=(
NAMED_UNIT(*)
PLANE_ANGLE_UNIT()
SI_UNIT($,.RADIAN.)
);
#20100=(
NAMED_UNIT(*)
SI_UNIT($,.STERADIAN.)
SOLID_ANGLE_UNIT()
);
#20125=SHAPE_DEFINITION_REPRESENTATION(#20183,#20336);
#20183=PRODUCT_DEFINITION_SHAPE('',$,#20390);
#20336=SHAPE_REPRESENTATION('',(#12121),#20067);
#20365=PRODUCT_DEFINITION_CONTEXT('part definition',#20526,'design');
#20390=PRODUCT_DEFINITION('M5x17.5 extrusion screw',
'M5x17.5 extrusion screw',#20443,#20365);
#20443=PRODUCT_DEFINITION_FORMATION('',$,#20552);
#20526=APPLICATION_CONTEXT(
'Core Data for Automotive Mechanical Design Process');
#20527=PRODUCT_CONTEXT('part definition',#20526,'mechanical');
#20552=PRODUCT('M5x17.5 extrusion screw','M5x17.5 extrusion screw',
'M5x17.5 extrusion screw',(#20527));
#20651=COLOUR_RGB('Black',0.12,0.14,0.17);
#20652=FILL_AREA_STYLE_COLOUR('',#20651);
#20653=FILL_AREA_STYLE('',(#20652));
#20654=SURFACE_STYLE_FILL_AREA(#20653);
#20655=SURFACE_SIDE_STYLE('',(#20654));
#20656=SURFACE_STYLE_USAGE(.BOTH.,#20655);
#20657=PRESENTATION_STYLE_ASSIGNMENT((#20656));
ENDSEC;
END-ISO-10303-21;
